ISO-10303-21;
HEADER;
/* Generated by software containing ST-Developer
 * from STEP Tools, Inc. (www.steptools.com) 
 */

FILE_DESCRIPTION(
/* description */ (''),
/* implementation_level */ '2;1');

FILE_NAME(
/* name */ '13_Taper_Roller_Bearing_30205_Cup.step',
/* time_stamp */ '2026-10-23T00:52:27+05:00',
/* author */ (''),
/* organization */ (''),
/* preprocessor_version */ 'ST-DEVELOPER v20.2',
/* originating_system */ 'Autodesk Translation Framework v15.15.0.0',
/* authorisation */ '');

FILE_SCHEMA (('AUTOMOTIVE_DESIGN { 1 0 10303 214 3 1 1 }'));
ENDSEC;

DATA;
#10=MECHANICAL_DESIGN_GEOMETRIC_PRESENTATION_REPRESENTATION('',(#1571),#59204);
#1524=SHAPE_REPRESENTATION_RELATIONSHIP('SRR','None',#59313,#1544);
#1544=ADVANCED_BREP_SHAPE_REPRESENTATION('',(#1591),#59200);
#1571=STYLED_ITEM('',(#59586),#1591);
#1591=MANIFOLD_SOLID_BREP('Cup',#22820);
#1796=FACE_BOUND('',#5187,.T.);
#1797=FACE_BOUND('',#5192,.T.);
#2230=PLANE('',#24623);
#2231=PLANE('',#24631);
#2582=CYLINDRICAL_SURFACE('',#24627,2.6);
#3683=FACE_OUTER_BOUND('',#5185,.T.);
#3684=FACE_OUTER_BOUND('',#5186,.T.);
#3685=FACE_OUTER_BOUND('',#5188,.T.);
#3686=FACE_OUTER_BOUND('',#5189,.T.);
#3687=FACE_OUTER_BOUND('',#5190,.T.);
#3688=FACE_OUTER_BOUND('',#5191,.T.);
#3689=FACE_OUTER_BOUND('',#5193,.T.);
#3690=FACE_OUTER_BOUND('',#5194,.T.);
#5185=EDGE_LOOP('',(#19834,#19835,#19836,#19837));
#5186=EDGE_LOOP('',(#19838));
#5187=EDGE_LOOP('',(#19839));
#5188=EDGE_LOOP('',(#19840,#19841,#19842,#19843));
#5189=EDGE_LOOP('',(#19844,#19845,#19846,#19847));
#5190=EDGE_LOOP('',(#19848,#19849,#19850,#19851));
#5191=EDGE_LOOP('',(#19852));
#5192=EDGE_LOOP('',(#19853));
#5193=EDGE_LOOP('',(#19854,#19855,#19856,#19857));
#5194=EDGE_LOOP('',(#19858,#19859,#19860,#19861));
#6538=LINE('',#48484,#7971);
#6539=LINE('',#48492,#7972);
#6540=LINE('',#48496,#7973);
#6541=LINE('',#48500,#7974);
#6542=LINE('',#48506,#7975);
#6543=LINE('',#48509,#7976);
#7971=VECTOR('',#29318,2.40256617975257);
#7972=VECTOR('',#29329,2.57);
#7973=VECTOR('',#29334,2.6);
#7974=VECTOR('',#29339,2.57);
#7975=VECTOR('',#29346,2.09090617619859);
#7976=VECTOR('',#29351,2.22173617797558);
#9025=CIRCLE('',#24621,2.37133297968149);
#9026=CIRCLE('',#24622,2.43379937982364);
#9027=CIRCLE('',#24624,2.54);
#9028=CIRCLE('',#24626,2.6);
#9029=CIRCLE('',#24628,2.6);
#9030=CIRCLE('',#24630,2.54);
#9031=CIRCLE('',#24632,2.10967297612751);
#9032=CIRCLE('',#24634,2.07213937626967);
#10869=VERTEX_POINT('',#48481);
#10870=VERTEX_POINT('',#48483);
#10871=VERTEX_POINT('',#48487);
#10872=VERTEX_POINT('',#48490);
#10873=VERTEX_POINT('',#48494);
#10874=VERTEX_POINT('',#48498);
#10875=VERTEX_POINT('',#48502);
#10876=VERTEX_POINT('',#48505);
#13921=EDGE_CURVE('',#10869,#10869,#9025,.T.);
#13922=EDGE_CURVE('',#10869,#10870,#6538,.T.);
#13923=EDGE_CURVE('',#10870,#10870,#9026,.T.);
#13924=EDGE_CURVE('',#10871,#10871,#9027,.T.);
#13925=EDGE_CURVE('',#10872,#10872,#9028,.T.);
#13926=EDGE_CURVE('',#10872,#10871,#6539,.T.);
#13927=EDGE_CURVE('',#10873,#10873,#9029,.T.);
#13928=EDGE_CURVE('',#10873,#10872,#6540,.T.);
#13929=EDGE_CURVE('',#10874,#10874,#9030,.T.);
#13930=EDGE_CURVE('',#10874,#10873,#6541,.T.);
#13931=EDGE_CURVE('',#10875,#10875,#9031,.T.);
#13932=EDGE_CURVE('',#10875,#10876,#6542,.T.);
#13933=EDGE_CURVE('',#10876,#10876,#9032,.T.);
#13934=EDGE_CURVE('',#10876,#10869,#6543,.T.);
#19834=ORIENTED_EDGE('',*,*,#13921,.T.);
#19835=ORIENTED_EDGE('',*,*,#13922,.T.);
#19836=ORIENTED_EDGE('',*,*,#13923,.F.);
#19837=ORIENTED_EDGE('',*,*,#13922,.F.);
#19838=ORIENTED_EDGE('',*,*,#13924,.F.);
#19839=ORIENTED_EDGE('',*,*,#13923,.T.);
#19840=ORIENTED_EDGE('',*,*,#13925,.F.);
#19841=ORIENTED_EDGE('',*,*,#13926,.T.);
#19842=ORIENTED_EDGE('',*,*,#13924,.T.);
#19843=ORIENTED_EDGE('',*,*,#13926,.F.);
#19844=ORIENTED_EDGE('',*,*,#13927,.F.);
#19845=ORIENTED_EDGE('',*,*,#13928,.T.);
#19846=ORIENTED_EDGE('',*,*,#13925,.T.);
#19847=ORIENTED_EDGE('',*,*,#13928,.F.);
#19848=ORIENTED_EDGE('',*,*,#13929,.F.);
#19849=ORIENTED_EDGE('',*,*,#13930,.T.);
#19850=ORIENTED_EDGE('',*,*,#13927,.T.);
#19851=ORIENTED_EDGE('',*,*,#13930,.F.);
#19852=ORIENTED_EDGE('',*,*,#13929,.T.);
#19853=ORIENTED_EDGE('',*,*,#13931,.F.);
#19854=ORIENTED_EDGE('',*,*,#13931,.T.);
#19855=ORIENTED_EDGE('',*,*,#13932,.T.);
#19856=ORIENTED_EDGE('',*,*,#13933,.F.);
#19857=ORIENTED_EDGE('',*,*,#13932,.F.);
#19858=ORIENTED_EDGE('',*,*,#13933,.T.);
#19859=ORIENTED_EDGE('',*,*,#13934,.T.);
#19860=ORIENTED_EDGE('',*,*,#13921,.F.);
#19861=ORIENTED_EDGE('',*,*,#13934,.F.);
#21485=CONICAL_SURFACE('',#24620,2.40256617975257,0.895793055792162);
#21486=CONICAL_SURFACE('',#24625,2.57,0.785398163397449);
#21487=CONICAL_SURFACE('',#24629,2.57,0.785398163397448);
#21488=CONICAL_SURFACE('',#24633,2.09090617619859,0.643931048266465);
#21489=CONICAL_SURFACE('',#24635,2.22173617797558,0.244346095279207);
#22513=ADVANCED_FACE('',(#3683),#21485,.F.);
#22514=ADVANCED_FACE('',(#3684,#1796),#2230,.T.);
#22515=ADVANCED_FACE('',(#3685),#21486,.T.);
#22516=ADVANCED_FACE('',(#3686),#2582,.T.);
#22517=ADVANCED_FACE('',(#3687),#21487,.T.);
#22518=ADVANCED_FACE('',(#3688,#1797),#2231,.T.);
#22519=ADVANCED_FACE('',(#3689),#21488,.F.);
#22520=ADVANCED_FACE('',(#3690),#21489,.F.);
#22820=CLOSED_SHELL('',(#22513,#22514,#22515,#22516,#22517,#22518,#22519,
#22520));
#24619=AXIS2_PLACEMENT_3D('',#48479,#29312,#29313);
#24620=AXIS2_PLACEMENT_3D('',#48480,#29314,#29315);
#24621=AXIS2_PLACEMENT_3D('',#48482,#29316,#29317);
#24622=AXIS2_PLACEMENT_3D('',#48485,#29319,#29320);
#24623=AXIS2_PLACEMENT_3D('',#48486,#29321,#29322);
#24624=AXIS2_PLACEMENT_3D('',#48488,#29323,#29324);
#24625=AXIS2_PLACEMENT_3D('',#48489,#29325,#29326);
#24626=AXIS2_PLACEMENT_3D('',#48491,#29327,#29328);
#24627=AXIS2_PLACEMENT_3D('',#48493,#29330,#29331);
#24628=AXIS2_PLACEMENT_3D('',#48495,#29332,#29333);
#24629=AXIS2_PLACEMENT_3D('',#48497,#29335,#29336);
#24630=AXIS2_PLACEMENT_3D('',#48499,#29337,#29338);
#24631=AXIS2_PLACEMENT_3D('',#48501,#29340,#29341);
#24632=AXIS2_PLACEMENT_3D('',#48503,#29342,#29343);
#24633=AXIS2_PLACEMENT_3D('',#48504,#29344,#29345);
#24634=AXIS2_PLACEMENT_3D('',#48507,#29347,#29348);
#24635=AXIS2_PLACEMENT_3D('',#48508,#29349,#29350);
#29312=DIRECTION('axis',(0.,0.,1.));
#29313=DIRECTION('refdir',(1.,0.,0.));
#29314=DIRECTION('center_axis',(0.,0.,-1.));
#29315=DIRECTION('ref_axis',(1.,0.,0.));
#29316=DIRECTION('center_axis',(0.,0.,1.));
#29317=DIRECTION('ref_axis',(1.,0.,0.));
#29318=DIRECTION('',(-0.780704907087438,-9.56087765543263E-17,-0.624899870418929));
#29319=DIRECTION('center_axis',(0.,0.,1.));
#29320=DIRECTION('ref_axis',(1.,0.,0.));
#29321=DIRECTION('center_axis',(0.,0.,-1.));
#29322=DIRECTION('ref_axis',(-1.,0.,0.));
#29323=DIRECTION('center_axis',(0.,0.,1.));
#29324=DIRECTION('ref_axis',(1.,0.,0.));
#29325=DIRECTION('center_axis',(0.,0.,1.));
#29326=DIRECTION('ref_axis',(1.,0.,0.));
#29327=DIRECTION('center_axis',(0.,0.,1.));
#29328=DIRECTION('ref_axis',(1.,0.,0.));
#29329=DIRECTION('',(0.707106781186548,8.65956056235494E-17,-0.707106781186547));
#29330=DIRECTION('center_axis',(0.,0.,1.));
#29331=DIRECTION('ref_axis',(1.,0.,0.));
#29332=DIRECTION('center_axis',(0.,0.,1.));
#29333=DIRECTION('ref_axis',(1.,0.,0.));
#29334=DIRECTION('',(0.,0.,-1.));
#29335=DIRECTION('center_axis',(0.,0.,-1.));
#29336=DIRECTION('ref_axis',(1.,0.,0.));
#29337=DIRECTION('center_axis',(0.,0.,1.));
#29338=DIRECTION('ref_axis',(1.,0.,0.));
#29339=DIRECTION('',(-0.707106781186548,-8.65956056235493E-17,-0.707106781186548));
#29340=DIRECTION('center_axis',(0.,0.,1.));
#29341=DIRECTION('ref_axis',(1.,0.,0.));
#29342=DIRECTION('center_axis',(0.,0.,1.));
#29343=DIRECTION('ref_axis',(1.,0.,0.));
#29344=DIRECTION('center_axis',(0.,0.,1.));
#29345=DIRECTION('ref_axis',(1.,0.,0.));
#29346=DIRECTION('',(0.600343896113564,7.35209230763127E-17,-0.79974196238486));
#29347=DIRECTION('center_axis',(0.,0.,1.));
#29348=DIRECTION('ref_axis',(1.,0.,0.));
#29349=DIRECTION('center_axis',(0.,0.,-1.));
#29350=DIRECTION('ref_axis',(1.,0.,0.));
#29351=DIRECTION('',(-0.241921895599668,-2.96268875089794E-17,-0.970295726275996));
#48479=CARTESIAN_POINT('',(0.,0.,0.));
#48480=CARTESIAN_POINT('Origin',(0.,0.,0.35));
#48481=CARTESIAN_POINT('',(-2.37133297968149,-2.90404534327949E-16,0.375));
#48482=CARTESIAN_POINT('Origin',(0.,0.,0.375));
#48483=CARTESIAN_POINT('',(-2.43379937982364,-2.98054462026784E-16,0.325));
#48484=CARTESIAN_POINT('',(-2.40256617975257,-2.94229498177366E-16,0.35));
#48485=CARTESIAN_POINT('Origin',(0.,0.,0.325));
#48486=CARTESIAN_POINT('Origin',(2.54,0.,0.325));
#48487=CARTESIAN_POINT('',(-2.54,-3.11060286983428E-16,0.325));
#48488=CARTESIAN_POINT('Origin',(0.,0.,0.325));
#48489=CARTESIAN_POINT('Origin',(0.,0.,0.355));
#48490=CARTESIAN_POINT('',(-2.6,-3.18408167778312E-16,0.385));
#48491=CARTESIAN_POINT('Origin',(0.,0.,0.385));
#48492=CARTESIAN_POINT('',(-2.57,-3.1473422738087E-16,0.355));
#48493=CARTESIAN_POINT('Origin',(0.,0.,0.975));
#48494=CARTESIAN_POINT('',(-2.6,-3.18408167778312E-16,1.565));
#48495=CARTESIAN_POINT('Origin',(0.,0.,1.565));
#48496=CARTESIAN_POINT('',(-2.6,-3.18408167778312E-16,0.975));
#48497=CARTESIAN_POINT('Origin',(0.,0.,1.595));
#48498=CARTESIAN_POINT('',(-2.54,-3.11060286983428E-16,1.625));
#48499=CARTESIAN_POINT('Origin',(0.,0.,1.625));
#48500=CARTESIAN_POINT('',(-2.57,-3.1473422738087E-16,1.595));
#48501=CARTESIAN_POINT('Origin',(2.10967297612751,0.,1.625));
#48502=CARTESIAN_POINT('',(-2.10967297612751,-2.58360425746223E-16,1.625));
#48503=CARTESIAN_POINT('Origin',(0.,0.,1.625));
#48504=CARTESIAN_POINT('Origin',(0.,0.,1.6));
#48505=CARTESIAN_POINT('',(-2.07213937626967,-2.53763885453584E-16,1.575));
#48506=CARTESIAN_POINT('',(-2.09090617619859,-2.56062155599903E-16,1.6));
#48507=CARTESIAN_POINT('Origin',(0.,0.,1.575));
#48508=CARTESIAN_POINT('Origin',(0.,0.,0.975));
#48509=CARTESIAN_POINT('',(-2.22173617797558,-2.72084209890766E-16,0.975));
#59178=UNCERTAINTY_MEASURE_WITH_UNIT(LENGTH_MEASURE(0.001),#59205,
'DISTANCE_ACCURACY_VALUE',
'Maximum model space distance between geometric entities at asserted c
onnectivities');
#59182=UNCERTAINTY_MEASURE_WITH_UNIT(LENGTH_MEASURE(0.001),#59205,
'DISTANCE_ACCURACY_VALUE',
'Maximum model space distance between geometric entities at asserted c
onnectivities');
#59200=(
GEOMETRIC_REPRESENTATION_CONTEXT(3)
GLOBAL_UNCERTAINTY_ASSIGNED_CONTEXT((#59178))
GLOBAL_UNIT_ASSIGNED_CONTEXT((#59205,#59207,#59208))
REPRESENTATION_CONTEXT('','3D')
);
#59204=(
GEOMETRIC_REPRESENTATION_CONTEXT(3)
GLOBAL_UNCERTAINTY_ASSIGNED_CONTEXT((#59182))
GLOBAL_UNIT_ASSIGNED_CONTEXT((#59205,#59207,#59208))
REPRESENTATION_CONTEXT('','3D')
);
#59205=(
LENGTH_UNIT()
NAMED_UNIT(*)
SI_UNIT(.CENTI.,.METRE.)
);
#59207=(
NAMED_UNIT(*)
PLANE_ANGLE_UNIT()
SI_UNIT($,.RADIAN.)
);
#59208=(
NAMED_UNIT(*)
SI_UNIT($,.STERADIAN.)
SOLID_ANGLE_UNIT()
);
#59226=SHAPE_DEFINITION_REPRESENTATION(#59247,#59313);
#59247=PRODUCT_DEFINITION_SHAPE('',$,#59335);
#59313=SHAPE_REPRESENTATION('',(#24619),#59200);
#59317=PRODUCT_DEFINITION_CONTEXT('part definition',#59382,'design');
#59335=PRODUCT_DEFINITION('2026-10-23-00-47-30-002',
'13_Taper_Roller_Bearing_30205_Cup',#59356,#59317);
#59356=PRODUCT_DEFINITION_FORMATION('',$,#59401);
#59382=APPLICATION_CONTEXT(
'Core Data for Automotive Mechanical Design Process');
#59383=PRODUCT_CONTEXT('part definition',#59382,'mechanical');
#59401=PRODUCT('2026-10-23-00-47-30-002',
'13_Taper_Roller_Bearing_30205_Cup',$,(#59383));
#59580=COLOUR_RGB('Grey',0.48,0.52,0.57);
#59581=FILL_AREA_STYLE_COLOUR('',#59580);
#59582=FILL_AREA_STYLE('',(#59581));
#59583=SURFACE_STYLE_FILL_AREA(#59582);
#59584=SURFACE_SIDE_STYLE('',(#59583));
#59585=SURFACE_STYLE_USAGE(.BOTH.,#59584);
#59586=PRESENTATION_STYLE_ASSIGNMENT((#59585));
ENDSEC;
END-ISO-10303-21;
